ISO-10303-21;
HEADER;
/* Generated by software containing ST-Developer
 * from STEP Tools, Inc. (www.steptools.com) 
 */

FILE_DESCRIPTION(
/* description */ ('Fatigue rig crank-slider'),
/* implementation_level */ '2;1');

FILE_NAME(
/* name */ 'Bearing bolt reducer.step',
/* time_stamp */ '2026-10-28T03:24:50-07:00',
/* author */ (''),
/* organization */ (''),
/* preprocessor_version */ 'ST-DEVELOPER v20.2',
/* originating_system */ 'Autodesk Translation Framework v15.17.0.0',
/* authorisation */ '');

FILE_SCHEMA (('AUTOMOTIVE_DESIGN { 1 0 10303 214 3 1 1 }'));
ENDSEC;

DATA;
#10=MECHANICAL_DESIGN_GEOMETRIC_PRESENTATION_REPRESENTATION('',(#589),#16911);
#489=SHAPE_REPRESENTATION_RELATIONSHIP('SRR','None',#17128,#539);
#539=ADVANCED_BREP_SHAPE_REPRESENTATION('',(#648),#16857);
#589=STYLED_ITEM('',(#17494),#648);
#648=MANIFOLD_SOLID_BREP('Body1',#8880);
#738=FACE_BOUND('',#1821,.T.);
#739=FACE_BOUND('',#1823,.T.);
#915=PLANE('',#9588);
#916=PLANE('',#9589);
#1257=FACE_OUTER_BOUND('',#1818,.T.);
#1258=FACE_OUTER_BOUND('',#1819,.T.);
#1259=FACE_OUTER_BOUND('',#1820,.T.);
#1260=FACE_OUTER_BOUND('',#1822,.T.);
#1818=EDGE_LOOP('',(#6176,#6177,#6178,#6179));
#1819=EDGE_LOOP('',(#6180,#6181,#6182,#6183));
#1820=EDGE_LOOP('',(#6184));
#1821=EDGE_LOOP('',(#6185));
#1822=EDGE_LOOP('',(#6186));
#1823=EDGE_LOOP('',(#6187));
#2506=LINE('',#13557,#3152);
#2507=LINE('',#13563,#3153);
#3152=VECTOR('',#10794,0.425);
#3153=VECTOR('',#10801,0.645);
#3796=CIRCLE('',#9583,0.425);
#3797=CIRCLE('',#9584,0.425);
#3798=CIRCLE('',#9586,0.645);
#3799=CIRCLE('',#9587,0.645);
#4212=VERTEX_POINT('',#13554);
#4213=VERTEX_POINT('',#13556);
#4214=VERTEX_POINT('',#13560);
#4215=VERTEX_POINT('',#13562);
#4986=EDGE_CURVE('',#4212,#4212,#3796,.T.);
#4987=EDGE_CURVE('',#4212,#4213,#2506,.T.);
#4988=EDGE_CURVE('',#4213,#4213,#3797,.T.);
#4989=EDGE_CURVE('',#4214,#4214,#3798,.T.);
#4990=EDGE_CURVE('',#4214,#4215,#2507,.T.);
#4991=EDGE_CURVE('',#4215,#4215,#3799,.T.);
#6176=ORIENTED_EDGE('',*,*,#4986,.F.);
#6177=ORIENTED_EDGE('',*,*,#4987,.T.);
#6178=ORIENTED_EDGE('',*,*,#4988,.T.);
#6179=ORIENTED_EDGE('',*,*,#4987,.F.);
#6180=ORIENTED_EDGE('',*,*,#4989,.F.);
#6181=ORIENTED_EDGE('',*,*,#4990,.T.);
#6182=ORIENTED_EDGE('',*,*,#4991,.T.);
#6183=ORIENTED_EDGE('',*,*,#4990,.F.);
#6184=ORIENTED_EDGE('',*,*,#4989,.T.);
#6185=ORIENTED_EDGE('',*,*,#4986,.T.);
#6186=ORIENTED_EDGE('',*,*,#4991,.F.);
#6187=ORIENTED_EDGE('',*,*,#4988,.F.);
#8218=CYLINDRICAL_SURFACE('',#9582,0.425);
#8219=CYLINDRICAL_SURFACE('',#9585,0.645);
#8395=ADVANCED_FACE('',(#1257),#8218,.F.);
#8396=ADVANCED_FACE('',(#1258),#8219,.T.);
#8397=ADVANCED_FACE('',(#1259,#738),#915,.T.);
#8398=ADVANCED_FACE('',(#1260,#739),#916,.F.);
#8880=CLOSED_SHELL('',(#8395,#8396,#8397,#8398));
#9581=AXIS2_PLACEMENT_3D('',#13552,#10788,#10789);
#9582=AXIS2_PLACEMENT_3D('',#13553,#10790,#10791);
#9583=AXIS2_PLACEMENT_3D('',#13555,#10792,#10793);
#9584=AXIS2_PLACEMENT_3D('',#13558,#10795,#10796);
#9585=AXIS2_PLACEMENT_3D('',#13559,#10797,#10798);
#9586=AXIS2_PLACEMENT_3D('',#13561,#10799,#10800);
#9587=AXIS2_PLACEMENT_3D('',#13564,#10802,#10803);
#9588=AXIS2_PLACEMENT_3D('',#13565,#10804,#10805);
#9589=AXIS2_PLACEMENT_3D('',#13566,#10806,#10807);
#10788=DIRECTION('axis',(0.,0.,1.));
#10789=DIRECTION('refdir',(1.,0.,0.));
#10790=DIRECTION('center_axis',(0.,0.,1.));
#10791=DIRECTION('ref_axis',(1.,0.,0.));
#10792=DIRECTION('center_axis',(0.,0.,-1.));
#10793=DIRECTION('ref_axis',(1.,0.,0.));
#10794=DIRECTION('',(0.,0.,-1.));
#10795=DIRECTION('center_axis',(0.,0.,-1.));
#10796=DIRECTION('ref_axis',(1.,0.,0.));
#10797=DIRECTION('center_axis',(0.,0.,1.));
#10798=DIRECTION('ref_axis',(1.,0.,0.));
#10799=DIRECTION('center_axis',(0.,0.,1.));
#10800=DIRECTION('ref_axis',(1.,0.,0.));
#10801=DIRECTION('',(0.,0.,-1.));
#10802=DIRECTION('center_axis',(0.,0.,1.));
#10803=DIRECTION('ref_axis',(1.,0.,0.));
#10804=DIRECTION('center_axis',(0.,0.,1.));
#10805=DIRECTION('ref_axis',(1.,0.,0.));
#10806=DIRECTION('center_axis',(0.,0.,1.));
#10807=DIRECTION('ref_axis',(1.,0.,0.));
#13552=CARTESIAN_POINT('',(0.,0.,0.));
#13553=CARTESIAN_POINT('Origin',(-4.75,-15.,8.67));
#13554=CARTESIAN_POINT('',(-5.175,-15.,9.87));
#13555=CARTESIAN_POINT('Origin',(-4.75,-15.,9.87));
#13556=CARTESIAN_POINT('',(-5.175,-15.,8.67));
#13557=CARTESIAN_POINT('',(-5.175,-15.,8.67));
#13558=CARTESIAN_POINT('Origin',(-4.75,-15.,8.67));
#13559=CARTESIAN_POINT('Origin',(-4.75,-15.,8.67));
#13560=CARTESIAN_POINT('',(-5.395,-15.,9.87));
#13561=CARTESIAN_POINT('Origin',(-4.75,-15.,9.87));
#13562=CARTESIAN_POINT('',(-5.395,-15.,8.67));
#13563=CARTESIAN_POINT('',(-5.395,-15.,8.67));
#13564=CARTESIAN_POINT('Origin',(-4.75,-15.,8.67));
#13565=CARTESIAN_POINT('Origin',(-4.75,-15.,9.87));
#13566=CARTESIAN_POINT('Origin',(-4.75,-15.,8.67));
#16798=UNCERTAINTY_MEASURE_WITH_UNIT(LENGTH_MEASURE(0.001),#16912,
'DISTANCE_ACCURACY_VALUE',
'Maximum model space distance between geometric entities at asserted c
onnectivities');
#16852=UNCERTAINTY_MEASURE_WITH_UNIT(LENGTH_MEASURE(0.001),#16912,
'DISTANCE_ACCURACY_VALUE',
'Maximum model space distance between geometric entities at asserted c
onnectivities');
#16857=(
GEOMETRIC_REPRESENTATION_CONTEXT(3)
GLOBAL_UNCERTAINTY_ASSIGNED_CONTEXT((#16798))
GLOBAL_UNIT_ASSIGNED_CONTEXT((#16912,#16914,#16915))
REPRESENTATION_CONTEXT('','3D')
);
#16911=(
GEOMETRIC_REPRESENTATION_CONTEXT(3)
GLOBAL_UNCERTAINTY_ASSIGNED_CONTEXT((#16852))
GLOBAL_UNIT_ASSIGNED_CONTEXT((#16912,#16914,#16915))
REPRESENTATION_CONTEXT('','3D')
);
#16912=(
LENGTH_UNIT()
NAMED_UNIT(*)
SI_UNIT(.CENTI.,.METRE.)
);
#16914=(
NAMED_UNIT(*)
PLANE_ANGLE_UNIT()
SI_UNIT($,.RADIAN.)
);
#16915=(
NAMED_UNIT(*)
SI_UNIT($,.STERADIAN.)
SOLID_ANGLE_UNIT()
);
#16920=SHAPE_DEFINITION_REPRESENTATION(#16978,#17128);
#16978=PRODUCT_DEFINITION_SHAPE('',$,#17187);
#17128=SHAPE_REPRESENTATION('',(#9581),#16857);
#17182=PRODUCT_DEFINITION_CONTEXT('part definition',#17358,'design');
#17187=PRODUCT_DEFINITION('Bearing bolt reducer','Bearing bolt reducer',
#17245,#17182);
#17245=PRODUCT_DEFINITION_FORMATION('',$,#17364);
#17358=APPLICATION_CONTEXT(
'Core Data for Automotive Mechanical Design Process');
#17359=PRODUCT_CONTEXT('part definition',#17358,'mechanical');
#17364=PRODUCT('Bearing bolt reducer','Bearing bolt reducer',
'Bearing bolt reducer',(#17359));
#17488=COLOUR_RGB('Black',0.12,0.14,0.17);
#17489=FILL_AREA_STYLE_COLOUR('',#17488);
#17490=FILL_AREA_STYLE('',(#17489));
#17491=SURFACE_STYLE_FILL_AREA(#17490);
#17492=SURFACE_SIDE_STYLE('',(#17491));
#17493=SURFACE_STYLE_USAGE(.BOTH.,#17492);
#17494=PRESENTATION_STYLE_ASSIGNMENT((#17493));
ENDSEC;
END-ISO-10303-21;
